ISO-10303-21;
HEADER;
/* Generated by software containing ST-Developer
 * from STEP Tools, Inc. (www.steptools.com) 
 */

FILE_DESCRIPTION(
/* description */ ('Turntable on roller ring'),
/* implementation_level */ '2;1');

FILE_NAME(
/* name */ 'Roller tread (1).step',
/* time_stamp */ '2026-10-28T03:23:59-07:00',
/* author */ (''),
/* organization */ (''),
/* preprocessor_version */ 'ST-DEVELOPER v20.2',
/* originating_system */ 'Autodesk Translation Framework v15.17.0.0',
/* authorisation */ '');

FILE_SCHEMA (('AUTOMOTIVE_DESIGN { 1 0 10303 214 3 1 1 }'));
ENDSEC;

DATA;
#10=MECHANICAL_DESIGN_GEOMETRIC_PRESENTATION_REPRESENTATION('',(#667),#16281);
#548=SHAPE_REPRESENTATION_RELATIONSHIP('SRR','None',#16570,#603);
#603=ADVANCED_BREP_SHAPE_REPRESENTATION('',(#735),#16264);
#667=STYLED_ITEM('',(#16925),#735);
#735=MANIFOLD_SOLID_BREP('Body1',#8412);
#963=FACE_BOUND('',#2382,.T.);
#964=FACE_BOUND('',#2384,.T.);
#1215=PLANE('',#9964);
#1216=PLANE('',#9965);
#1668=FACE_OUTER_BOUND('',#2379,.T.);
#1669=FACE_OUTER_BOUND('',#2380,.T.);
#1670=FACE_OUTER_BOUND('',#2381,.T.);
#1671=FACE_OUTER_BOUND('',#2383,.T.);
#2379=EDGE_LOOP('',(#7349,#7350,#7351,#7352));
#2380=EDGE_LOOP('',(#7353,#7354,#7355,#7356));
#2381=EDGE_LOOP('',(#7357));
#2382=EDGE_LOOP('',(#7358));
#2383=EDGE_LOOP('',(#7359));
#2384=EDGE_LOOP('',(#7360));
#2942=LINE('',#15400,#3425);
#2943=LINE('',#15406,#3426);
#3425=VECTOR('',#12489,1.5);
#3426=VECTOR('',#12496,2.);
#3841=CIRCLE('',#9959,1.5);
#3842=CIRCLE('',#9960,1.5);
#3843=CIRCLE('',#9962,2.);
#3844=CIRCLE('',#9963,2.);
#4517=VERTEX_POINT('',#15397);
#4518=VERTEX_POINT('',#15399);
#4519=VERTEX_POINT('',#15403);
#4520=VERTEX_POINT('',#15405);
#5485=EDGE_CURVE('',#4517,#4517,#3841,.T.);
#5486=EDGE_CURVE('',#4517,#4518,#2942,.T.);
#5487=EDGE_CURVE('',#4518,#4518,#3842,.T.);
#5488=EDGE_CURVE('',#4519,#4519,#3843,.T.);
#5489=EDGE_CURVE('',#4519,#4520,#2943,.T.);
#5490=EDGE_CURVE('',#4520,#4520,#3844,.T.);
#7349=ORIENTED_EDGE('',*,*,#5485,.F.);
#7350=ORIENTED_EDGE('',*,*,#5486,.T.);
#7351=ORIENTED_EDGE('',*,*,#5487,.T.);
#7352=ORIENTED_EDGE('',*,*,#5486,.F.);
#7353=ORIENTED_EDGE('',*,*,#5488,.F.);
#7354=ORIENTED_EDGE('',*,*,#5489,.T.);
#7355=ORIENTED_EDGE('',*,*,#5490,.T.);
#7356=ORIENTED_EDGE('',*,*,#5489,.F.);
#7357=ORIENTED_EDGE('',*,*,#5488,.T.);
#7358=ORIENTED_EDGE('',*,*,#5485,.T.);
#7359=ORIENTED_EDGE('',*,*,#5490,.F.);
#7360=ORIENTED_EDGE('',*,*,#5487,.F.);
#7823=CYLINDRICAL_SURFACE('',#9958,1.5);
#7824=CYLINDRICAL_SURFACE('',#9961,2.);
#8271=ADVANCED_FACE('',(#1668),#7823,.F.);
#8272=ADVANCED_FACE('',(#1669),#7824,.T.);
#8273=ADVANCED_FACE('',(#1670,#963),#1215,.T.);
#8274=ADVANCED_FACE('',(#1671,#964),#1216,.F.);
#8412=CLOSED_SHELL('',(#8271,#8272,#8273,#8274));
#9957=AXIS2_PLACEMENT_3D('',#15395,#12483,#12484);
#9958=AXIS2_PLACEMENT_3D('',#15396,#12485,#12486);
#9959=AXIS2_PLACEMENT_3D('',#15398,#12487,#12488);
#9960=AXIS2_PLACEMENT_3D('',#15401,#12490,#12491);
#9961=AXIS2_PLACEMENT_3D('',#15402,#12492,#12493);
#9962=AXIS2_PLACEMENT_3D('',#15404,#12494,#12495);
#9963=AXIS2_PLACEMENT_3D('',#15407,#12497,#12498);
#9964=AXIS2_PLACEMENT_3D('',#15408,#12499,#12500);
#9965=AXIS2_PLACEMENT_3D('',#15409,#12501,#12502);
#12483=DIRECTION('axis',(0.,0.,1.));
#12484=DIRECTION('refdir',(1.,0.,0.));
#12485=DIRECTION('center_axis',(0.,1.,0.));
#12486=DIRECTION('ref_axis',(1.,0.,0.));
#12487=DIRECTION('center_axis',(0.,-1.,0.));
#12488=DIRECTION('ref_axis',(1.,0.,0.));
#12489=DIRECTION('',(0.,-1.,0.));
#12490=DIRECTION('center_axis',(0.,-1.,0.));
#12491=DIRECTION('ref_axis',(1.,0.,0.));
#12492=DIRECTION('center_axis',(0.,1.,0.));
#12493=DIRECTION('ref_axis',(1.,0.,0.));
#12494=DIRECTION('center_axis',(0.,1.,0.));
#12495=DIRECTION('ref_axis',(1.,0.,0.));
#12496=DIRECTION('',(0.,-1.,0.));
#12497=DIRECTION('center_axis',(0.,1.,0.));
#12498=DIRECTION('ref_axis',(1.,0.,0.));
#12499=DIRECTION('center_axis',(0.,1.,0.));
#12500=DIRECTION('ref_axis',(1.,0.,0.));
#12501=DIRECTION('center_axis',(0.,1.,0.));
#12502=DIRECTION('ref_axis',(1.,0.,0.));
#15395=CARTESIAN_POINT('',(0.,0.,0.));
#15396=CARTESIAN_POINT('Origin',(0.,14.35,3.5));
#15397=CARTESIAN_POINT('',(-1.5,15.65,3.5));
#15398=CARTESIAN_POINT('Origin',(0.,15.65,3.5));
#15399=CARTESIAN_POINT('',(-1.5,14.35,3.5));
#15400=CARTESIAN_POINT('',(-1.5,14.35,3.5));
#15401=CARTESIAN_POINT('Origin',(0.,14.35,3.5));
#15402=CARTESIAN_POINT('Origin',(0.,14.35,3.5));
#15403=CARTESIAN_POINT('',(-2.,15.65,3.5));
#15404=CARTESIAN_POINT('Origin',(0.,15.65,3.5));
#15405=CARTESIAN_POINT('',(-2.,14.35,3.5));
#15406=CARTESIAN_POINT('',(-2.,14.35,3.5));
#15407=CARTESIAN_POINT('Origin',(0.,14.35,3.5));
#15408=CARTESIAN_POINT('Origin',(0.,15.65,3.5));
#15409=CARTESIAN_POINT('Origin',(0.,14.35,3.5));
#16195=UNCERTAINTY_MEASURE_WITH_UNIT(LENGTH_MEASURE(0.001),#16282,
'DISTANCE_ACCURACY_VALUE',
'Maximum model space distance between geometric entities at asserted c
onnectivities');
#16212=UNCERTAINTY_MEASURE_WITH_UNIT(LENGTH_MEASURE(0.001),#16282,
'DISTANCE_ACCURACY_VALUE',
'Maximum model space distance between geometric entities at asserted c
onnectivities');
#16264=(
GEOMETRIC_REPRESENTATION_CONTEXT(3)
GLOBAL_UNCERTAINTY_ASSIGNED_CONTEXT((#16195))
GLOBAL_UNIT_ASSIGNED_CONTEXT((#16282,#16284,#16285))
REPRESENTATION_CONTEXT('','3D')
);
#16281=(
GEOMETRIC_REPRESENTATION_CONTEXT(3)
GLOBAL_UNCERTAINTY_ASSIGNED_CONTEXT((#16212))
GLOBAL_UNIT_ASSIGNED_CONTEXT((#16282,#16284,#16285))
REPRESENTATION_CONTEXT('','3D')
);
#16282=(
LENGTH_UNIT()
NAMED_UNIT(*)
SI_UNIT(.CENTI.,.METRE.)
);
#16284=(
NAMED_UNIT(*)
PLANE_ANGLE_UNIT()
SI_UNIT($,.RADIAN.)
);
#16285=(
NAMED_UNIT(*)
SI_UNIT($,.STERADIAN.)
SOLID_ANGLE_UNIT()
);
#16337=SHAPE_DEFINITION_REPRESENTATION(#16471,#16570);
#16471=PRODUCT_DEFINITION_SHAPE('',$,#16639);
#16570=SHAPE_REPRESENTATION('',(#9957),#16264);
#16587=PRODUCT_DEFINITION_CONTEXT('part definition',#16793,'design');
#16639=PRODUCT_DEFINITION('Roller tread (1)','Roller tread (1)',#16707,#16587);
#16707=PRODUCT_DEFINITION_FORMATION('',$,#16846);
#16793=APPLICATION_CONTEXT(
'Core Data for Automotive Mechanical Design Process');
#16794=PRODUCT_CONTEXT('part definition',#16793,'mechanical');
#16846=PRODUCT('Roller tread (1)','Roller tread (1)','Roller tread (1)',(#16794));
#16919=COLOUR_RGB('Sky Blue',0.24,0.69,0.87);
#16920=FILL_AREA_STYLE_COLOUR('',#16919);
#16921=FILL_AREA_STYLE('',(#16920));
#16922=SURFACE_STYLE_FILL_AREA(#16921);
#16923=SURFACE_SIDE_STYLE('',(#16922));
#16924=SURFACE_STYLE_USAGE(.BOTH.,#16923);
#16925=PRESENTATION_STYLE_ASSIGNMENT((#16924));
ENDSEC;
END-ISO-10303-21;
